ISO-10303-21;
HEADER;
/* Generated by software containing ST-Developer
 * from STEP Tools, Inc. (www.steptools.com) 
 */

FILE_DESCRIPTION(
/* description */ ('STEP AP214'),
/* implementation_level */ '2;1');

FILE_NAME(
/* name */ 'Wall Flange Rosette (1).step',
/* time_stamp */ '2026-10-05T23:18:41-07:00',
/* author */ (''),
/* organization */ (''),
/* preprocessor_version */ 'ST-DEVELOPER v20.2',
/* originating_system */ 'Autodesk Translation Framework v15.15.0.0',
/* authorisation */ '');

FILE_SCHEMA (('AUTOMOTIVE_DESIGN { 1 0 10303 214 3 1 1 }'));
ENDSEC;

DATA;
#10=MECHANICAL_DESIGN_GEOMETRIC_PRESENTATION_REPRESENTATION('',(#109),#221662);
#70=MANIFOLD_SOLID_BREP('Body1',#79332);
#83=SHAPE_REPRESENTATION_RELATIONSHIP('SRR','None',#221718,#96);
#96=ADVANCED_BREP_SHAPE_REPRESENTATION('',(#70),#221658);
#109=STYLED_ITEM('',(#221783),#70);
#314=FACE_BOUND('',#24933,.T.);
#315=FACE_BOUND('',#24935,.T.);
#316=FACE_BOUND('',#24937,.T.);
#317=FACE_BOUND('',#24940,.T.);
#318=FACE_BOUND('',#24942,.T.);
#1903=TOROIDAL_SURFACE('',#80952,26.5,1.);
#1904=TOROIDAL_SURFACE('',#80964,26.5,0.5);
#1956=CONICAL_SURFACE('',#80970,15.31367390024,0.849141474959914);
#1957=CONICAL_SURFACE('',#80977,15.125,0.849141474959914);
#2273=CYLINDRICAL_SURFACE('',#80956,27.5);
#2274=CYLINDRICAL_SURFACE('',#80958,12.4);
#2275=CYLINDRICAL_SURFACE('',#80961,2.00000000000001);
#2276=CYLINDRICAL_SURFACE('',#80968,27.);
#3220=LINE('',#183766,#10287);
#3221=LINE('',#183773,#10288);
#3222=LINE('',#183776,#10289);
#3223=LINE('',#183789,#10290);
#3224=LINE('',#183794,#10291);
#3225=LINE('',#183803,#10292);
#10287=VECTOR('',#89633,27.5);
#10288=VECTOR('',#89640,1000.);
#10289=VECTOR('',#89643,1000.);
#10290=VECTOR('',#89662,27.);
#10291=VECTOR('',#89667,15.31367390024);
#10292=VECTOR('',#89680,15.125);
#17018=PLANE('',#80973);
#17019=PLANE('',#80974);
#17020=PLANE('',#80975);
#17021=PLANE('',#80979);
#17022=PLANE('',#80980);
#20841=FACE_OUTER_BOUND('',#24925,.T.);
#20842=FACE_OUTER_BOUND('',#24926,.T.);
#20843=FACE_OUTER_BOUND('',#24927,.T.);
#20844=FACE_OUTER_BOUND('',#24928,.T.);
#20845=FACE_OUTER_BOUND('',#24929,.T.);
#20846=FACE_OUTER_BOUND('',#24930,.T.);
#20847=FACE_OUTER_BOUND('',#24931,.T.);
#20848=FACE_OUTER_BOUND('',#24932,.T.);
#20849=FACE_OUTER_BOUND('',#24934,.T.);
#20850=FACE_OUTER_BOUND('',#24936,.T.);
#20851=FACE_OUTER_BOUND('',#24938,.T.);
#20852=FACE_OUTER_BOUND('',#24939,.T.);
#20853=FACE_OUTER_BOUND('',#24941,.T.);
#24925=EDGE_LOOP('',(#57127,#57128,#57129,#57130));
#24926=EDGE_LOOP('',(#57131,#57132,#57133,#57134));
#24927=EDGE_LOOP('',(#57135,#57136,#57137,#57138));
#24928=EDGE_LOOP('',(#57139,#57140,#57141,#57142));
#24929=EDGE_LOOP('',(#57143,#57144,#57145,#57146));
#24930=EDGE_LOOP('',(#57147,#57148,#57149,#57150));
#24931=EDGE_LOOP('',(#57151,#57152,#57153,#57154));
#24932=EDGE_LOOP('',(#57155));
#24933=EDGE_LOOP('',(#57156));
#24934=EDGE_LOOP('',(#57157));
#24935=EDGE_LOOP('',(#57158,#57159));
#24936=EDGE_LOOP('',(#57160));
#24937=EDGE_LOOP('',(#57161,#57162));
#24938=EDGE_LOOP('',(#57163,#57164,#57165,#57166));
#24939=EDGE_LOOP('',(#57167));
#24940=EDGE_LOOP('',(#57168));
#24941=EDGE_LOOP('',(#57169));
#24942=EDGE_LOOP('',(#57170));
#31391=CIRCLE('',#80953,26.49999955823);
#31392=CIRCLE('',#80954,1.);
#31393=CIRCLE('',#80955,27.5);
#31394=CIRCLE('',#80957,27.5);
#31395=CIRCLE('',#80959,12.4);
#31396=CIRCLE('',#80960,12.4);
#31397=CIRCLE('',#80962,2.);
#31398=CIRCLE('',#80963,2.);
#31399=CIRCLE('',#80965,27.);
#31400=CIRCLE('',#80966,0.5);
#31401=CIRCLE('',#80967,26.5);
#31402=CIRCLE('',#80969,27.);
#31403=CIRCLE('',#80971,15.93867390024);
#31404=CIRCLE('',#80972,14.68867390024);
#31405=CIRCLE('',#80976,14.5);
#31406=CIRCLE('',#80978,15.75);
#35014=VERTEX_POINT('',#183759);
#35015=VERTEX_POINT('',#183761);
#35016=VERTEX_POINT('',#183765);
#35017=VERTEX_POINT('',#183769);
#35018=VERTEX_POINT('',#183770);
#35019=VERTEX_POINT('',#183772);
#35020=VERTEX_POINT('',#183774);
#35021=VERTEX_POINT('',#183781);
#35022=VERTEX_POINT('',#183783);
#35023=VERTEX_POINT('',#183787);
#35024=VERTEX_POINT('',#183791);
#35025=VERTEX_POINT('',#183793);
#35026=VERTEX_POINT('',#183799);
#35027=VERTEX_POINT('',#183802);
#43396=EDGE_CURVE('',#35014,#35014,#31391,.T.);
#43397=EDGE_CURVE('',#35014,#35015,#31392,.T.);
#43398=EDGE_CURVE('',#35015,#35015,#31393,.T.);
#43399=EDGE_CURVE('',#35015,#35016,#3220,.T.);
#43400=EDGE_CURVE('',#35016,#35016,#31394,.T.);
#43401=EDGE_CURVE('',#35017,#35018,#31395,.T.);
#43402=EDGE_CURVE('',#35019,#35017,#3221,.T.);
#43403=EDGE_CURVE('',#35019,#35020,#31396,.T.);
#43404=EDGE_CURVE('',#35020,#35018,#3222,.T.);
#43405=EDGE_CURVE('',#35018,#35017,#31397,.T.);
#43406=EDGE_CURVE('',#35020,#35019,#31398,.T.);
#43407=EDGE_CURVE('',#35021,#35021,#31399,.T.);
#43408=EDGE_CURVE('',#35021,#35022,#31400,.T.);
#43409=EDGE_CURVE('',#35022,#35022,#31401,.T.);
#43410=EDGE_CURVE('',#35023,#35023,#31402,.T.);
#43411=EDGE_CURVE('',#35023,#35021,#3223,.T.);
#43412=EDGE_CURVE('',#35024,#35024,#31403,.T.);
#43413=EDGE_CURVE('',#35024,#35025,#3224,.T.);
#43414=EDGE_CURVE('',#35025,#35025,#31404,.T.);
#43415=EDGE_CURVE('',#35026,#35026,#31405,.T.);
#43416=EDGE_CURVE('',#35026,#35027,#3225,.T.);
#43417=EDGE_CURVE('',#35027,#35027,#31406,.T.);
#57127=ORIENTED_EDGE('',*,*,#43396,.F.);
#57128=ORIENTED_EDGE('',*,*,#43397,.T.);
#57129=ORIENTED_EDGE('',*,*,#43398,.T.);
#57130=ORIENTED_EDGE('',*,*,#43397,.F.);
#57131=ORIENTED_EDGE('',*,*,#43398,.F.);
#57132=ORIENTED_EDGE('',*,*,#43399,.T.);
#57133=ORIENTED_EDGE('',*,*,#43400,.T.);
#57134=ORIENTED_EDGE('',*,*,#43399,.F.);
#57135=ORIENTED_EDGE('',*,*,#43401,.F.);
#57136=ORIENTED_EDGE('',*,*,#43402,.F.);
#57137=ORIENTED_EDGE('',*,*,#43403,.T.);
#57138=ORIENTED_EDGE('',*,*,#43404,.T.);
#57139=ORIENTED_EDGE('',*,*,#43405,.F.);
#57140=ORIENTED_EDGE('',*,*,#43404,.F.);
#57141=ORIENTED_EDGE('',*,*,#43406,.T.);
#57142=ORIENTED_EDGE('',*,*,#43402,.T.);
#57143=ORIENTED_EDGE('',*,*,#43407,.F.);
#57144=ORIENTED_EDGE('',*,*,#43408,.T.);
#57145=ORIENTED_EDGE('',*,*,#43409,.T.);
#57146=ORIENTED_EDGE('',*,*,#43408,.F.);
#57147=ORIENTED_EDGE('',*,*,#43410,.F.);
#57148=ORIENTED_EDGE('',*,*,#43411,.T.);
#57149=ORIENTED_EDGE('',*,*,#43407,.T.);
#57150=ORIENTED_EDGE('',*,*,#43411,.F.);
#57151=ORIENTED_EDGE('',*,*,#43412,.F.);
#57152=ORIENTED_EDGE('',*,*,#43413,.T.);
#57153=ORIENTED_EDGE('',*,*,#43414,.T.);
#57154=ORIENTED_EDGE('',*,*,#43413,.F.);
#57155=ORIENTED_EDGE('',*,*,#43409,.F.);
#57156=ORIENTED_EDGE('',*,*,#43412,.T.);
#57157=ORIENTED_EDGE('',*,*,#43414,.F.);
#57158=ORIENTED_EDGE('',*,*,#43406,.F.);
#57159=ORIENTED_EDGE('',*,*,#43403,.F.);
#57160=ORIENTED_EDGE('',*,*,#43415,.T.);
#57161=ORIENTED_EDGE('',*,*,#43405,.T.);
#57162=ORIENTED_EDGE('',*,*,#43401,.T.);
#57163=ORIENTED_EDGE('',*,*,#43415,.F.);
#57164=ORIENTED_EDGE('',*,*,#43416,.T.);
#57165=ORIENTED_EDGE('',*,*,#43417,.T.);
#57166=ORIENTED_EDGE('',*,*,#43416,.F.);
#57167=ORIENTED_EDGE('',*,*,#43396,.T.);
#57168=ORIENTED_EDGE('',*,*,#43417,.F.);
#57169=ORIENTED_EDGE('',*,*,#43400,.F.);
#57170=ORIENTED_EDGE('',*,*,#43410,.T.);
#76271=ADVANCED_FACE('',(#20841),#1903,.T.);
#76272=ADVANCED_FACE('',(#20842),#2273,.T.);
#76273=ADVANCED_FACE('',(#20843),#2274,.F.);
#76274=ADVANCED_FACE('',(#20844),#2275,.F.);
#76275=ADVANCED_FACE('',(#20845),#1904,.F.);
#76276=ADVANCED_FACE('',(#20846),#2276,.F.);
#76277=ADVANCED_FACE('',(#20847),#1956,.T.);
#76278=ADVANCED_FACE('',(#20848,#314),#17018,.F.);
#76279=ADVANCED_FACE('',(#20849,#315),#17019,.F.);
#76280=ADVANCED_FACE('',(#20850,#316),#17020,.T.);
#76281=ADVANCED_FACE('',(#20851),#1957,.F.);
#76282=ADVANCED_FACE('',(#20852,#317),#17021,.T.);
#76283=ADVANCED_FACE('',(#20853,#318),#17022,.F.);
#79332=CLOSED_SHELL('',(#76271,#76272,#76273,#76274,#76275,#76276,#76277,
#76278,#76279,#76280,#76281,#76282,#76283));
#80951=AXIS2_PLACEMENT_3D('',#183757,#89621,#89622);
#80952=AXIS2_PLACEMENT_3D('',#183758,#89623,#89624);
#80953=AXIS2_PLACEMENT_3D('',#183760,#89625,#89626);
#80954=AXIS2_PLACEMENT_3D('',#183762,#89627,#89628);
#80955=AXIS2_PLACEMENT_3D('',#183763,#89629,#89630);
#80956=AXIS2_PLACEMENT_3D('',#183764,#89631,#89632);
#80957=AXIS2_PLACEMENT_3D('',#183767,#89634,#89635);
#80958=AXIS2_PLACEMENT_3D('',#183768,#89636,#89637);
#80959=AXIS2_PLACEMENT_3D('',#183771,#89638,#89639);
#80960=AXIS2_PLACEMENT_3D('',#183775,#89641,#89642);
#80961=AXIS2_PLACEMENT_3D('',#183777,#89644,#89645);
#80962=AXIS2_PLACEMENT_3D('',#183778,#89646,#89647);
#80963=AXIS2_PLACEMENT_3D('',#183779,#89648,#89649);
#80964=AXIS2_PLACEMENT_3D('',#183780,#89650,#89651);
#80965=AXIS2_PLACEMENT_3D('',#183782,#89652,#89653);
#80966=AXIS2_PLACEMENT_3D('',#183784,#89654,#89655);
#80967=AXIS2_PLACEMENT_3D('',#183785,#89656,#89657);
#80968=AXIS2_PLACEMENT_3D('',#183786,#89658,#89659);
#80969=AXIS2_PLACEMENT_3D('',#183788,#89660,#89661);
#80970=AXIS2_PLACEMENT_3D('',#183790,#89663,#89664);
#80971=AXIS2_PLACEMENT_3D('',#183792,#89665,#89666);
#80972=AXIS2_PLACEMENT_3D('',#183795,#89668,#89669);
#80973=AXIS2_PLACEMENT_3D('',#183796,#89670,#89671);
#80974=AXIS2_PLACEMENT_3D('',#183797,#89672,#89673);
#80975=AXIS2_PLACEMENT_3D('',#183798,#89674,#89675);
#80976=AXIS2_PLACEMENT_3D('',#183800,#89676,#89677);
#80977=AXIS2_PLACEMENT_3D('',#183801,#89678,#89679);
#80978=AXIS2_PLACEMENT_3D('',#183804,#89681,#89682);
#80979=AXIS2_PLACEMENT_3D('',#183805,#89683,#89684);
#80980=AXIS2_PLACEMENT_3D('',#183806,#89685,#89686);
#89621=DIRECTION('axis',(0.,0.,1.));
#89622=DIRECTION('refdir',(1.,0.,0.));
#89623=DIRECTION('center_axis',(1.,0.,0.));
#89624=DIRECTION('ref_axis',(0.,0.924224592736303,0.381849318686593));
#89625=DIRECTION('center_axis',(1.,0.,0.));
#89626=DIRECTION('ref_axis',(0.,0.381849318686592,-0.924224592736303));
#89627=DIRECTION('center_axis',(0.,0.381849318686593,-0.924224592736303));
#89628=DIRECTION('ref_axis',(0.,-0.924224592736303,-0.381849318686593));
#89629=DIRECTION('center_axis',(1.,0.,0.));
#89630=DIRECTION('ref_axis',(0.,0.381849318686593,-0.924224592736303));
#89631=DIRECTION('center_axis',(1.,0.,0.));
#89632=DIRECTION('ref_axis',(0.,0.924224592736303,0.381849318686593));
#89633=DIRECTION('',(-1.,0.,0.));
#89634=DIRECTION('center_axis',(1.,0.,0.));
#89635=DIRECTION('ref_axis',(0.,0.381849318686593,-0.924224592736303));
#89636=DIRECTION('center_axis',(-1.,0.,0.));
#89637=DIRECTION('ref_axis',(0.,0.381849318686586,-0.924224592736306));
#89638=DIRECTION('center_axis',(-1.,0.,0.));
#89639=DIRECTION('ref_axis',(0.,-0.228299548172813,0.973590938897897));
#89640=DIRECTION('',(1.,0.,0.));
#89641=DIRECTION('center_axis',(-1.,0.,0.));
#89642=DIRECTION('ref_axis',(0.,-0.228299548172813,0.973590938897897));
#89643=DIRECTION('',(1.,0.,0.));
#89644=DIRECTION('center_axis',(-1.,0.,0.));
#89645=DIRECTION('ref_axis',(0.,-0.381849318686584,0.924224592736306));
#89646=DIRECTION('center_axis',(-1.,0.,0.));
#89647=DIRECTION('ref_axis',(0.,-0.890419977397047,-0.455139828901232));
#89648=DIRECTION('center_axis',(-1.,0.,0.));
#89649=DIRECTION('ref_axis',(0.,-0.890419977397047,-0.455139828901232));
#89650=DIRECTION('center_axis',(1.,0.,0.));
#89651=DIRECTION('ref_axis',(0.,0.924224592736303,0.381849318686593));
#89652=DIRECTION('center_axis',(1.,0.,0.));
#89653=DIRECTION('ref_axis',(0.,0.381849318686593,-0.924224592736303));
#89654=DIRECTION('center_axis',(0.,-0.381849318686593,0.924224592736303));
#89655=DIRECTION('ref_axis',(0.,-0.924224592736303,-0.381849318686593));
#89656=DIRECTION('center_axis',(1.,0.,0.));
#89657=DIRECTION('ref_axis',(0.,0.381849318686592,-0.924224592736303));
#89658=DIRECTION('center_axis',(1.,0.,0.));
#89659=DIRECTION('ref_axis',(0.,0.924224592736303,0.381849318686593));
#89660=DIRECTION('center_axis',(1.,0.,0.));
#89661=DIRECTION('ref_axis',(0.,0.381849318686593,-0.924224592736303));
#89662=DIRECTION('',(1.,0.,0.));
#89663=DIRECTION('center_axis',(1.,-4.17636281571063E-17,-1.72549108550083E-17));
#89664=DIRECTION('ref_axis',(4.51877481786748E-17,0.924224592736303,0.381849318686593));
#89665=DIRECTION('center_axis',(1.,0.,0.));
#89666=DIRECTION('ref_axis',(0.,-0.924224592736303,-0.381849318686593));
#89667=DIRECTION('',(-0.660627895620383,0.693827893847184,0.286659444721022));
#89668=DIRECTION('center_axis',(1.,0.,0.));
#89669=DIRECTION('ref_axis',(0.,0.924224592736303,0.381849318686593));
#89670=DIRECTION('center_axis',(1.,0.,0.));
#89671=DIRECTION('ref_axis',(0.,1.,0.));
#89672=DIRECTION('center_axis',(1.,0.,0.));
#89673=DIRECTION('ref_axis',(0.,1.,0.));
#89674=DIRECTION('center_axis',(1.,0.,0.));
#89675=DIRECTION('ref_axis',(0.,1.,0.));
#89676=DIRECTION('center_axis',(1.,0.,0.));
#89677=DIRECTION('ref_axis',(0.,0.924224592736303,0.381849318686593));
#89678=DIRECTION('center_axis',(1.,2.78469808118585E-18,1.15051587396146E-18));
#89679=DIRECTION('ref_axis',(-3.01301015258785E-18,0.924224592736303,0.381849318686593));
#89680=DIRECTION('',(0.660627895620383,-0.693827893847184,-0.286659444721022));
#89681=DIRECTION('center_axis',(1.,0.,0.));
#89682=DIRECTION('ref_axis',(0.,0.924224592736303,0.381849318686592));
#89683=DIRECTION('center_axis',(1.,0.,0.));
#89684=DIRECTION('ref_axis',(0.,1.,0.));
#89685=DIRECTION('center_axis',(1.,0.,0.));
#89686=DIRECTION('ref_axis',(0.,1.,0.));
#183757=CARTESIAN_POINT('',(0.,0.,0.));
#183758=CARTESIAN_POINT('Origin',(-30.5675339847409,-75.,72.98888938658));
#183759=CARTESIAN_POINT('',(-29.5675339847409,-99.4919512992173,62.8698826100749));
#183760=CARTESIAN_POINT('Origin',(-29.5675339847409,-75.,72.98888938658));
#183761=CARTESIAN_POINT('',(-30.5675339847409,-100.416176300248,62.4880331226987));
#183762=CARTESIAN_POINT('Origin',(-30.5675339847409,-99.491951707512,62.8698824413853));
#183763=CARTESIAN_POINT('Origin',(-30.5675339847409,-75.,72.98888938658));
#183764=CARTESIAN_POINT('Origin',(-50.5675339847409,-75.,72.98888938658));
#183765=CARTESIAN_POINT('',(-50.5675339847409,-100.416176300248,62.4880331226987));
#183766=CARTESIAN_POINT('',(-50.5675339847409,-100.416176300248,62.4880331226987));
#183767=CARTESIAN_POINT('Origin',(-50.5675339847409,-75.,72.98888938658));
#183768=CARTESIAN_POINT('Origin',(-50.5675339847409,-75.,72.98888938658));
#183769=CARTESIAN_POINT('',(-30.6675339847409,-77.8309143973437,85.0614170289143));
#183770=CARTESIAN_POINT('',(-30.6675339847409,-81.5157715065078,83.5389946787084));
#183771=CARTESIAN_POINT('Origin',(-30.6675339847409,-75.,72.98888938658));
#183772=CARTESIAN_POINT('',(-31.1675339847409,-77.8309143973437,85.0614170289143));
#183773=CARTESIAN_POINT('',(-31.1675339847409,-77.8309143973437,85.0614170289143));
#183774=CARTESIAN_POINT('',(-31.1675339847409,-81.5157715065078,83.5389946787084));
#183775=CARTESIAN_POINT('Origin',(-31.1675339847409,-75.,72.98888938658));
#183776=CARTESIAN_POINT('',(-31.1675339847409,-81.5157715065078,83.5389946787084));
#183777=CARTESIAN_POINT('Origin',(-50.5675339847409,-79.7349315517137,84.4492743365101));
#183778=CARTESIAN_POINT('Origin',(-30.6675339847409,-79.7349315517137,84.4492743365101));
#183779=CARTESIAN_POINT('Origin',(-31.1675339847409,-79.7349315517137,84.4492743365101));
#183780=CARTESIAN_POINT('Origin',(-30.5675339847409,-75.,72.98888938658));
#183781=CARTESIAN_POINT('',(-30.5675339847409,-99.9540640038802,62.678957782042));
#183782=CARTESIAN_POINT('Origin',(-30.5675339847409,-75.,72.98888938658));
#183783=CARTESIAN_POINT('',(-30.0675339847409,-99.491951707512,62.8698824413853));
#183784=CARTESIAN_POINT('Origin',(-30.5675339847409,-99.491951707512,62.8698824413853));
#183785=CARTESIAN_POINT('Origin',(-30.0675339847409,-75.,72.98888938658));
#183786=CARTESIAN_POINT('Origin',(-50.5675339847409,-75.,72.98888938658));
#183787=CARTESIAN_POINT('',(-50.5675339847409,-99.9540640038802,62.678957782042));
#183788=CARTESIAN_POINT('Origin',(-50.5675339847409,-75.,72.98888938658));
#183789=CARTESIAN_POINT('',(-50.5675339847409,-99.9540640038802,62.678957782042));
#183790=CARTESIAN_POINT('Origin',(-30.6175339847409,-75.,72.98888938658));
#183791=CARTESIAN_POINT('',(-30.0675339847409,-89.730914394206,66.9027176170056));
#183792=CARTESIAN_POINT('Origin',(-30.0675339847409,-75.,72.98888938658));
#183793=CARTESIAN_POINT('',(-31.1675339847409,-88.5756336532856,67.3800292653638));
#183794=CARTESIAN_POINT('',(-30.6175339847409,-89.1532740237459,67.1413734411847));
#183795=CARTESIAN_POINT('Origin',(-31.1675339847409,-75.,72.98888938658));
#183796=CARTESIAN_POINT('Origin',(-30.0675339847409,-75.,72.98888938658));
#183797=CARTESIAN_POINT('Origin',(-31.1675339847409,-75.,72.98888938658));
#183798=CARTESIAN_POINT('Origin',(-30.6675339847409,-75.,72.98888938658));
#183799=CARTESIAN_POINT('',(-30.6675339847409,-88.4012565946763,67.4520742656244));
#183800=CARTESIAN_POINT('Origin',(-30.6675339847409,-75.,72.98888938658));
#183801=CARTESIAN_POINT('Origin',(-30.1175339847409,-75.,72.98888938658));
#183802=CARTESIAN_POINT('',(-29.5675339847409,-89.5565373355967,66.9747626172662));
#183803=CARTESIAN_POINT('',(-30.1175339847409,-88.9788969651366,67.2134184414453));
#183804=CARTESIAN_POINT('Origin',(-29.5675339847409,-75.,72.98888938658));
#183805=CARTESIAN_POINT('Origin',(-29.5675339847409,-75.,72.98888938658));
#183806=CARTESIAN_POINT('Origin',(-50.5675339847409,-75.,72.98888938658));
#221643=UNCERTAINTY_MEASURE_WITH_UNIT(LENGTH_MEASURE(0.01),#221663,
'DISTANCE_ACCURACY_VALUE',
'Maximum model space distance between geometric entities at asserted c
onnectivities');
#221647=UNCERTAINTY_MEASURE_WITH_UNIT(LENGTH_MEASURE(0.01),#221663,
'DISTANCE_ACCURACY_VALUE',
'Maximum model space distance between geometric entities at asserted c
onnectivities');
#221658=(
GEOMETRIC_REPRESENTATION_CONTEXT(3)
GLOBAL_UNCERTAINTY_ASSIGNED_CONTEXT((#221643))
GLOBAL_UNIT_ASSIGNED_CONTEXT((#221663,#221665,#221666))
REPRESENTATION_CONTEXT('','3D')
);
#221662=(
GEOMETRIC_REPRESENTATION_CONTEXT(3)
GLOBAL_UNCERTAINTY_ASSIGNED_CONTEXT((#221647))
GLOBAL_UNIT_ASSIGNED_CONTEXT((#221663,#221665,#221666))
REPRESENTATION_CONTEXT('','3D')
);
#221663=(
LENGTH_UNIT()
NAMED_UNIT(*)
SI_UNIT(.MILLI.,.METRE.)
);
#221665=(
NAMED_UNIT(*)
PLANE_ANGLE_UNIT()
SI_UNIT($,.RADIAN.)
);
#221666=(
NAMED_UNIT(*)
SI_UNIT($,.STERADIAN.)
SOLID_ANGLE_UNIT()
);
#221677=SHAPE_DEFINITION_REPRESENTATION(#221691,#221718);
#221691=PRODUCT_DEFINITION_SHAPE('',$,#221733);
#221718=SHAPE_REPRESENTATION('',(#80951),#221658);
#221722=PRODUCT_DEFINITION_CONTEXT('part definition',#221766,'design');
#221733=PRODUCT_DEFINITION('2026-10-05-23-02-44-166',
'Wall Flange Rosette (1)',#221747,#221722);
#221747=PRODUCT_DEFINITION_FORMATION('',$,#221778);
#221766=APPLICATION_CONTEXT(
'Core Data for Automotive Mechanical Design Process');
#221767=PRODUCT_CONTEXT('part definition',#221766,'mechanical');
#221778=PRODUCT('2026-10-05-23-02-44-166','Wall Flange Rosette (1)',$,(#221767));
#221783=PRESENTATION_STYLE_ASSIGNMENT((#221785));
#221785=SURFACE_STYLE_USAGE(.BOTH.,#221787);
#221787=SURFACE_SIDE_STYLE('',(#221789));
#221789=SURFACE_STYLE_FILL_AREA(#221791);
#221791=FILL_AREA_STYLE('Opaque(202,209,238)',(#221793));
#221793=FILL_AREA_STYLE_COLOUR('Opaque(202,209,238)',#221795);
#221795=COLOUR_RGB('Opaque(202,209,238)', 0.09019608, 0.27058824, 0.51372549);
ENDSEC;
END-ISO-10303-21;
